ISO-10303-21;
HEADER;
/* Generated by software containing ST-Developer
 * from STEP Tools, Inc. (www.steptools.com) 
 */

FILE_DESCRIPTION(
/* description */ (''),
/* implementation_level */ '2;1');

FILE_NAME(
/* name */ 'Pivot thrust washer.step',
/* time_stamp */ '2026-11-10T09:05:57-08:00',
/* author */ (''),
/* organization */ (''),
/* preprocessor_version */ 'ST-DEVELOPER v20.2',
/* originating_system */ 'Autodesk Translation Framework v15.17.0.0',
/* authorisation */ '');

FILE_SCHEMA (('AUTOMOTIVE_DESIGN { 1 0 10303 214 3 1 1 }'));
ENDSEC;

DATA;
#10=MECHANICAL_DESIGN_GEOMETRIC_PRESENTATION_REPRESENTATION('',(#574),#19618);
#554=SHAPE_REPRESENTATION_RELATIONSHIP('SRR','None',#19674,#564);
#564=ADVANCED_BREP_SHAPE_REPRESENTATION('',(#584),#19617);
#574=STYLED_ITEM('',(#19734),#584);
#584=MANIFOLD_SOLID_BREP('Body1',#7112);
#658=FACE_BOUND('',#1695,.T.);
#659=FACE_BOUND('',#1697,.T.);
#819=PLANE('',#7759);
#820=PLANE('',#7760);
#1220=FACE_OUTER_BOUND('',#1692,.T.);
#1221=FACE_OUTER_BOUND('',#1693,.T.);
#1222=FACE_OUTER_BOUND('',#1694,.T.);
#1223=FACE_OUTER_BOUND('',#1696,.T.);
#1692=EDGE_LOOP('',(#6546,#6547,#6548,#6549));
#1693=EDGE_LOOP('',(#6550,#6551,#6552,#6553));
#1694=EDGE_LOOP('',(#6554));
#1695=EDGE_LOOP('',(#6555));
#1696=EDGE_LOOP('',(#6556));
#1697=EDGE_LOOP('',(#6557));
#2155=LINE('',#19575,#2614);
#2156=LINE('',#19581,#2615);
#2614=VECTOR('',#9288,0.41);
#2615=VECTOR('',#9295,0.6);
#2806=CIRCLE('',#7754,0.41);
#2807=CIRCLE('',#7755,0.41);
#2808=CIRCLE('',#7757,0.6);
#2809=CIRCLE('',#7758,0.6);
#3473=VERTEX_POINT('',#19572);
#3474=VERTEX_POINT('',#19574);
#3475=VERTEX_POINT('',#19578);
#3476=VERTEX_POINT('',#19580);
#4498=EDGE_CURVE('',#3473,#3473,#2806,.T.);
#4499=EDGE_CURVE('',#3473,#3474,#2155,.T.);
#4500=EDGE_CURVE('',#3474,#3474,#2807,.T.);
#4501=EDGE_CURVE('',#3475,#3475,#2808,.T.);
#4502=EDGE_CURVE('',#3475,#3476,#2156,.T.);
#4503=EDGE_CURVE('',#3476,#3476,#2809,.T.);
#6546=ORIENTED_EDGE('',*,*,#4498,.F.);
#6547=ORIENTED_EDGE('',*,*,#4499,.T.);
#6548=ORIENTED_EDGE('',*,*,#4500,.T.);
#6549=ORIENTED_EDGE('',*,*,#4499,.F.);
#6550=ORIENTED_EDGE('',*,*,#4501,.F.);
#6551=ORIENTED_EDGE('',*,*,#4502,.T.);
#6552=ORIENTED_EDGE('',*,*,#4503,.T.);
#6553=ORIENTED_EDGE('',*,*,#4502,.F.);
#6554=ORIENTED_EDGE('',*,*,#4501,.T.);
#6555=ORIENTED_EDGE('',*,*,#4498,.T.);
#6556=ORIENTED_EDGE('',*,*,#4503,.F.);
#6557=ORIENTED_EDGE('',*,*,#4500,.F.);
#6698=CYLINDRICAL_SURFACE('',#7753,0.41);
#6699=CYLINDRICAL_SURFACE('',#7756,0.6);
#7099=ADVANCED_FACE('',(#1220),#6698,.F.);
#7100=ADVANCED_FACE('',(#1221),#6699,.T.);
#7101=ADVANCED_FACE('',(#1222,#658),#819,.T.);
#7102=ADVANCED_FACE('',(#1223,#659),#820,.F.);
#7112=CLOSED_SHELL('',(#7099,#7100,#7101,#7102));
#7752=AXIS2_PLACEMENT_3D('',#19570,#9282,#9283);
#7753=AXIS2_PLACEMENT_3D('',#19571,#9284,#9285);
#7754=AXIS2_PLACEMENT_3D('',#19573,#9286,#9287);
#7755=AXIS2_PLACEMENT_3D('',#19576,#9289,#9290);
#7756=AXIS2_PLACEMENT_3D('',#19577,#9291,#9292);
#7757=AXIS2_PLACEMENT_3D('',#19579,#9293,#9294);
#7758=AXIS2_PLACEMENT_3D('',#19582,#9296,#9297);
#7759=AXIS2_PLACEMENT_3D('',#19583,#9298,#9299);
#7760=AXIS2_PLACEMENT_3D('',#19584,#9300,#9301);
#9282=DIRECTION('axis',(0.,0.,1.));
#9283=DIRECTION('refdir',(1.,0.,0.));
#9284=DIRECTION('center_axis',(0.,0.,1.));
#9285=DIRECTION('ref_axis',(1.,0.,0.));
#9286=DIRECTION('center_axis',(0.,0.,-1.));
#9287=DIRECTION('ref_axis',(1.,0.,0.));
#9288=DIRECTION('',(0.,0.,-1.));
#9289=DIRECTION('center_axis',(0.,0.,-1.));
#9290=DIRECTION('ref_axis',(1.,0.,0.));
#9291=DIRECTION('center_axis',(0.,0.,1.));
#9292=DIRECTION('ref_axis',(1.,0.,0.));
#9293=DIRECTION('center_axis',(0.,0.,1.));
#9294=DIRECTION('ref_axis',(1.,0.,0.));
#9295=DIRECTION('',(0.,0.,-1.));
#9296=DIRECTION('center_axis',(0.,0.,1.));
#9297=DIRECTION('ref_axis',(1.,0.,0.));
#9298=DIRECTION('center_axis',(0.,0.,1.));
#9299=DIRECTION('ref_axis',(1.,0.,0.));
#9300=DIRECTION('center_axis',(0.,0.,1.));
#9301=DIRECTION('ref_axis',(1.,0.,0.));
#19570=CARTESIAN_POINT('',(0.,0.,0.));
#19571=CARTESIAN_POINT('Origin',(0.,0.,0.));
#19572=CARTESIAN_POINT('',(-0.41,-5.02105187650415E-17,0.1));
#19573=CARTESIAN_POINT('Origin',(0.,0.,0.1));
#19574=CARTESIAN_POINT('',(-0.41,-5.02105187650415E-17,0.));
#19575=CARTESIAN_POINT('',(-0.41,-5.02105187650415E-17,0.));
#19576=CARTESIAN_POINT('Origin',(0.,0.,0.));
#19577=CARTESIAN_POINT('Origin',(0.,0.,0.));
#19578=CARTESIAN_POINT('',(-0.6,-7.34788079488412E-17,0.1));
#19579=CARTESIAN_POINT('Origin',(0.,0.,0.1));
#19580=CARTESIAN_POINT('',(-0.6,-7.34788079488412E-17,0.));
#19581=CARTESIAN_POINT('',(-0.6,-7.34788079488412E-17,0.));
#19582=CARTESIAN_POINT('Origin',(0.,0.,0.));
#19583=CARTESIAN_POINT('Origin',(0.,0.,0.1));
#19584=CARTESIAN_POINT('Origin',(0.,0.,0.));
#19604=UNCERTAINTY_MEASURE_WITH_UNIT(LENGTH_MEASURE(0.001),#19619,
'DISTANCE_ACCURACY_VALUE',
'Maximum model space distance between geometric entities at asserted c
onnectivities');
#19605=UNCERTAINTY_MEASURE_WITH_UNIT(LENGTH_MEASURE(0.001),#19619,
'DISTANCE_ACCURACY_VALUE',
'Maximum model space distance between geometric entities at asserted c
onnectivities');
#19617=(
GEOMETRIC_REPRESENTATION_CONTEXT(3)
GLOBAL_UNCERTAINTY_ASSIGNED_CONTEXT((#19604))
GLOBAL_UNIT_ASSIGNED_CONTEXT((#19619,#19621,#19622))
REPRESENTATION_CONTEXT('','3D')
);
#19618=(
GEOMETRIC_REPRESENTATION_CONTEXT(3)
GLOBAL_UNCERTAINTY_ASSIGNED_CONTEXT((#19605))
GLOBAL_UNIT_ASSIGNED_CONTEXT((#19619,#19621,#19622))
REPRESENTATION_CONTEXT('','3D')
);
#19619=(
LENGTH_UNIT()
NAMED_UNIT(*)
SI_UNIT(.CENTI.,.METRE.)
);
#19621=(
NAMED_UNIT(*)
PLANE_ANGLE_UNIT()
SI_UNIT($,.RADIAN.)
);
#19622=(
NAMED_UNIT(*)
SI_UNIT($,.STERADIAN.)
SOLID_ANGLE_UNIT()
);
#19634=SHAPE_DEFINITION_REPRESENTATION(#19654,#19674);
#19654=PRODUCT_DEFINITION_SHAPE('',$,#19687);
#19674=SHAPE_REPRESENTATION('',(#7752),#19617);
#19675=PRODUCT_DEFINITION_CONTEXT('part definition',#19713,'design');
#19687=PRODUCT_DEFINITION('Pivot thrust washer','Pivot thrust washer',#19699,
#19675);
#19699=PRODUCT_DEFINITION_FORMATION('',$,#19726);
#19713=APPLICATION_CONTEXT(
'Core Data for Automotive Mechanical Design Process');
#19714=PRODUCT_CONTEXT('part definition',#19713,'mechanical');
#19726=PRODUCT('Pivot thrust washer','Pivot thrust washer',$,(#19714));
#19734=PRESENTATION_STYLE_ASSIGNMENT((#19742));
#19742=SURFACE_STYLE_USAGE(.BOTH.,#19750);
#19750=SURFACE_SIDE_STYLE('',(#19758));
#19758=SURFACE_STYLE_FILL_AREA(#19766);
#19766=FILL_AREA_STYLE('Washer gray',(#19774));
#19774=FILL_AREA_STYLE_COLOUR('Washer gray',#19782);
#19782=COLOUR_RGB('Washer gray',0.725490196078431,0.752941176470588,0.792156862745098);
ENDSEC;
END-ISO-10303-21;
